ISO-10303-21;
HEADER;
/* Generated by software containing ST-Developer
 * from STEP Tools, Inc. (www.steptools.com) 
 */

FILE_DESCRIPTION(
/* description */ ('Turntable on roller ring'),
/* implementation_level */ '2;1');

FILE_NAME(
/* name */ 'Socket Set Screw - M5x8.step',
/* time_stamp */ '2026-10-28T03:23:59-07:00',
/* author */ (''),
/* organization */ (''),
/* preprocessor_version */ 'ST-DEVELOPER v20.2',
/* originating_system */ 'Autodesk Translation Framework v15.17.0.0',
/* authorisation */ '');

FILE_SCHEMA (('AUTOMOTIVE_DESIGN { 1 0 10303 214 3 1 1 }'));
ENDSEC;

DATA;
#10=MECHANICAL_DESIGN_GEOMETRIC_PRESENTATION_REPRESENTATION('',(#641),#16281);
#487=CONICAL_SURFACE('',#9518,0.235,0.785398163397448);
#488=CONICAL_SURFACE('',#9522,0.2125,0.785398163397448);
#522=SHAPE_REPRESENTATION_RELATIONSHIP('SRR','None',#16538,#577);
#577=ADVANCED_BREP_SHAPE_REPRESENTATION('',(#711),#16232);
#641=STYLED_ITEM('',(#16939),#711);
#711=MANIFOLD_SOLID_BREP('Body1',#8384);
#866=FACE_BOUND('',#2070,.T.);
#1074=PLANE('',#9509);
#1075=PLANE('',#9510);
#1076=PLANE('',#9511);
#1077=PLANE('',#9512);
#1078=PLANE('',#9513);
#1079=PLANE('',#9514);
#1080=PLANE('',#9515);
#1081=PLANE('',#9516);
#1082=PLANE('',#9524);
#1448=FACE_OUTER_BOUND('',#2062,.T.);
#1449=FACE_OUTER_BOUND('',#2063,.T.);
#1450=FACE_OUTER_BOUND('',#2064,.T.);
#1451=FACE_OUTER_BOUND('',#2065,.T.);
#1452=FACE_OUTER_BOUND('',#2066,.T.);
#1453=FACE_OUTER_BOUND('',#2067,.T.);
#1454=FACE_OUTER_BOUND('',#2068,.T.);
#1455=FACE_OUTER_BOUND('',#2069,.T.);
#1456=FACE_OUTER_BOUND('',#2071,.T.);
#1457=FACE_OUTER_BOUND('',#2072,.T.);
#1458=FACE_OUTER_BOUND('',#2073,.T.);
#1459=FACE_OUTER_BOUND('',#2074,.T.);
#2062=EDGE_LOOP('',(#6495,#6496,#6497,#6498));
#2063=EDGE_LOOP('',(#6499,#6500,#6501,#6502));
#2064=EDGE_LOOP('',(#6503,#6504,#6505,#6506));
#2065=EDGE_LOOP('',(#6507,#6508,#6509,#6510));
#2066=EDGE_LOOP('',(#6511,#6512,#6513,#6514));
#2067=EDGE_LOOP('',(#6515,#6516,#6517,#6518));
#2068=EDGE_LOOP('',(#6519,#6520,#6521,#6522,#6523,#6524));
#2069=EDGE_LOOP('',(#6525));
#2070=EDGE_LOOP('',(#6526,#6527,#6528,#6529,#6530,#6531));
#2071=EDGE_LOOP('',(#6532,#6533,#6534,#6535));
#2072=EDGE_LOOP('',(#6536,#6537,#6538,#6539));
#2073=EDGE_LOOP('',(#6540,#6541,#6542,#6543));
#2074=EDGE_LOOP('',(#6544));
#2665=LINE('',#14391,#3148);
#2666=LINE('',#14393,#3149);
#2667=LINE('',#14395,#3150);
#2668=LINE('',#14396,#3151);
#2669=LINE('',#14399,#3152);
#2670=LINE('',#14401,#3153);
#2671=LINE('',#14402,#3154);
#2672=LINE('',#14405,#3155);
#2673=LINE('',#14407,#3156);
#2674=LINE('',#14408,#3157);
#2675=LINE('',#14411,#3158);
#2676=LINE('',#14413,#3159);
#2677=LINE('',#14414,#3160);
#2678=LINE('',#14417,#3161);
#2679=LINE('',#14419,#3162);
#2680=LINE('',#14420,#3163);
#2681=LINE('',#14422,#3164);
#2682=LINE('',#14423,#3165);
#2683=LINE('',#14431,#3166);
#2684=LINE('',#14435,#3167);
#2685=LINE('',#14439,#3168);
#3148=VECTOR('',#11312,1.);
#3149=VECTOR('',#11313,1.);
#3150=VECTOR('',#11314,1.);
#3151=VECTOR('',#11315,1.);
#3152=VECTOR('',#11318,1.);
#3153=VECTOR('',#11319,1.);
#3154=VECTOR('',#11320,1.);
#3155=VECTOR('',#11323,1.);
#3156=VECTOR('',#11324,1.);
#3157=VECTOR('',#11325,1.);
#3158=VECTOR('',#11328,1.);
#3159=VECTOR('',#11329,1.);
#3160=VECTOR('',#11330,1.);
#3161=VECTOR('',#11333,1.);
#3162=VECTOR('',#11334,1.);
#3163=VECTOR('',#11335,1.);
#3164=VECTOR('',#11338,1.);
#3165=VECTOR('',#11339,1.);
#3166=VECTOR('',#11350,0.235);
#3167=VECTOR('',#11355,0.25);
#3168=VECTOR('',#11360,0.2125);
#3691=CIRCLE('',#9517,0.22);
#3692=CIRCLE('',#9519,0.24505);
#3693=CIRCLE('',#9521,0.24505);
#3694=CIRCLE('',#9523,0.175);
#4235=VERTEX_POINT('',#14389);
#4236=VERTEX_POINT('',#14390);
#4237=VERTEX_POINT('',#14392);
#4238=VERTEX_POINT('',#14394);
#4239=VERTEX_POINT('',#14398);
#4240=VERTEX_POINT('',#14400);
#4241=VERTEX_POINT('',#14404);
#4242=VERTEX_POINT('',#14406);
#4243=VERTEX_POINT('',#14410);
#4244=VERTEX_POINT('',#14412);
#4245=VERTEX_POINT('',#14416);
#4246=VERTEX_POINT('',#14418);
#4247=VERTEX_POINT('',#14426);
#4248=VERTEX_POINT('',#14429);
#4249=VERTEX_POINT('',#14433);
#4250=VERTEX_POINT('',#14437);
#5058=EDGE_CURVE('',#4235,#4236,#2665,.T.);
#5059=EDGE_CURVE('',#4235,#4237,#2666,.T.);
#5060=EDGE_CURVE('',#4237,#4238,#2667,.T.);
#5061=EDGE_CURVE('',#4236,#4238,#2668,.T.);
#5062=EDGE_CURVE('',#4239,#4235,#2669,.T.);
#5063=EDGE_CURVE('',#4239,#4240,#2670,.T.);
#5064=EDGE_CURVE('',#4240,#4237,#2671,.T.);
#5065=EDGE_CURVE('',#4241,#4239,#2672,.T.);
#5066=EDGE_CURVE('',#4241,#4242,#2673,.T.);
#5067=EDGE_CURVE('',#4242,#4240,#2674,.T.);
#5068=EDGE_CURVE('',#4243,#4241,#2675,.T.);
#5069=EDGE_CURVE('',#4243,#4244,#2676,.T.);
#5070=EDGE_CURVE('',#4244,#4242,#2677,.T.);
#5071=EDGE_CURVE('',#4245,#4243,#2678,.T.);
#5072=EDGE_CURVE('',#4245,#4246,#2679,.T.);
#5073=EDGE_CURVE('',#4246,#4244,#2680,.T.);
#5074=EDGE_CURVE('',#4236,#4245,#2681,.T.);
#5075=EDGE_CURVE('',#4238,#4246,#2682,.T.);
#5076=EDGE_CURVE('',#4247,#4247,#3691,.T.);
#5077=EDGE_CURVE('',#4248,#4248,#3692,.T.);
#5078=EDGE_CURVE('',#4248,#4247,#2683,.T.);
#5079=EDGE_CURVE('',#4249,#4249,#3693,.F.);
#5080=EDGE_CURVE('',#4249,#4248,#2684,.T.);
#5081=EDGE_CURVE('',#4250,#4250,#3694,.T.);
#5082=EDGE_CURVE('',#4250,#4249,#2685,.T.);
#6495=ORIENTED_EDGE('',*,*,#5058,.F.);
#6496=ORIENTED_EDGE('',*,*,#5059,.T.);
#6497=ORIENTED_EDGE('',*,*,#5060,.T.);
#6498=ORIENTED_EDGE('',*,*,#5061,.F.);
#6499=ORIENTED_EDGE('',*,*,#5062,.F.);
#6500=ORIENTED_EDGE('',*,*,#5063,.T.);
#6501=ORIENTED_EDGE('',*,*,#5064,.T.);
#6502=ORIENTED_EDGE('',*,*,#5059,.F.);
#6503=ORIENTED_EDGE('',*,*,#5065,.F.);
#6504=ORIENTED_EDGE('',*,*,#5066,.T.);
#6505=ORIENTED_EDGE('',*,*,#5067,.T.);
#6506=ORIENTED_EDGE('',*,*,#5063,.F.);
#6507=ORIENTED_EDGE('',*,*,#5068,.F.);
#6508=ORIENTED_EDGE('',*,*,#5069,.T.);
#6509=ORIENTED_EDGE('',*,*,#5070,.T.);
#6510=ORIENTED_EDGE('',*,*,#5066,.F.);
#6511=ORIENTED_EDGE('',*,*,#5071,.F.);
#6512=ORIENTED_EDGE('',*,*,#5072,.T.);
#6513=ORIENTED_EDGE('',*,*,#5073,.T.);
#6514=ORIENTED_EDGE('',*,*,#5069,.F.);
#6515=ORIENTED_EDGE('',*,*,#5074,.F.);
#6516=ORIENTED_EDGE('',*,*,#5061,.T.);
#6517=ORIENTED_EDGE('',*,*,#5075,.T.);
#6518=ORIENTED_EDGE('',*,*,#5072,.F.);
#6519=ORIENTED_EDGE('',*,*,#5075,.F.);
#6520=ORIENTED_EDGE('',*,*,#5060,.F.);
#6521=ORIENTED_EDGE('',*,*,#5064,.F.);
#6522=ORIENTED_EDGE('',*,*,#5067,.F.);
#6523=ORIENTED_EDGE('',*,*,#5070,.F.);
#6524=ORIENTED_EDGE('',*,*,#5073,.F.);
#6525=ORIENTED_EDGE('',*,*,#5076,.F.);
#6526=ORIENTED_EDGE('',*,*,#5058,.T.);
#6527=ORIENTED_EDGE('',*,*,#5074,.T.);
#6528=ORIENTED_EDGE('',*,*,#5071,.T.);
#6529=ORIENTED_EDGE('',*,*,#5068,.T.);
#6530=ORIENTED_EDGE('',*,*,#5065,.T.);
#6531=ORIENTED_EDGE('',*,*,#5062,.T.);
#6532=ORIENTED_EDGE('',*,*,#5077,.F.);
#6533=ORIENTED_EDGE('',*,*,#5078,.T.);
#6534=ORIENTED_EDGE('',*,*,#5076,.T.);
#6535=ORIENTED_EDGE('',*,*,#5078,.F.);
#6536=ORIENTED_EDGE('',*,*,#5079,.F.);
#6537=ORIENTED_EDGE('',*,*,#5080,.T.);
#6538=ORIENTED_EDGE('',*,*,#5077,.T.);
#6539=ORIENTED_EDGE('',*,*,#5080,.F.);
#6540=ORIENTED_EDGE('',*,*,#5081,.F.);
#6541=ORIENTED_EDGE('',*,*,#5082,.T.);
#6542=ORIENTED_EDGE('',*,*,#5079,.T.);
#6543=ORIENTED_EDGE('',*,*,#5082,.F.);
#6544=ORIENTED_EDGE('',*,*,#5081,.T.);
#7752=CYLINDRICAL_SURFACE('',#9520,0.24505);
#8051=ADVANCED_FACE('',(#1448),#1074,.F.);
#8052=ADVANCED_FACE('',(#1449),#1075,.F.);
#8053=ADVANCED_FACE('',(#1450),#1076,.F.);
#8054=ADVANCED_FACE('',(#1451),#1077,.F.);
#8055=ADVANCED_FACE('',(#1452),#1078,.F.);
#8056=ADVANCED_FACE('',(#1453),#1079,.F.);
#8057=ADVANCED_FACE('',(#1454),#1080,.F.);
#8058=ADVANCED_FACE('',(#1455,#866),#1081,.T.);
#8059=ADVANCED_FACE('',(#1456),#487,.T.);
#8060=ADVANCED_FACE('',(#1457),#7752,.T.);
#8061=ADVANCED_FACE('',(#1458),#488,.T.);
#8062=ADVANCED_FACE('',(#1459),#1082,.T.);
#8384=CLOSED_SHELL('',(#8051,#8052,#8053,#8054,#8055,#8056,#8057,#8058,
#8059,#8060,#8061,#8062));
#9508=AXIS2_PLACEMENT_3D('',#14387,#11308,#11309);
#9509=AXIS2_PLACEMENT_3D('',#14388,#11310,#11311);
#9510=AXIS2_PLACEMENT_3D('',#14397,#11316,#11317);
#9511=AXIS2_PLACEMENT_3D('',#14403,#11321,#11322);
#9512=AXIS2_PLACEMENT_3D('',#14409,#11326,#11327);
#9513=AXIS2_PLACEMENT_3D('',#14415,#11331,#11332);
#9514=AXIS2_PLACEMENT_3D('',#14421,#11336,#11337);
#9515=AXIS2_PLACEMENT_3D('',#14424,#11340,#11341);
#9516=AXIS2_PLACEMENT_3D('',#14425,#11342,#11343);
#9517=AXIS2_PLACEMENT_3D('',#14427,#11344,#11345);
#9518=AXIS2_PLACEMENT_3D('',#14428,#11346,#11347);
#9519=AXIS2_PLACEMENT_3D('',#14430,#11348,#11349);
#9520=AXIS2_PLACEMENT_3D('',#14432,#11351,#11352);
#9521=AXIS2_PLACEMENT_3D('',#14434,#11353,#11354);
#9522=AXIS2_PLACEMENT_3D('',#14436,#11356,#11357);
#9523=AXIS2_PLACEMENT_3D('',#14438,#11358,#11359);
#9524=AXIS2_PLACEMENT_3D('',#14440,#11361,#11362);
#11308=DIRECTION('axis',(0.,0.,1.));
#11309=DIRECTION('refdir',(1.,0.,0.));
#11310=DIRECTION('center_axis',(0.866025403784439,0.,-0.5));
#11311=DIRECTION('ref_axis',(0.5,0.,0.866025403784439));
#11312=DIRECTION('',(0.5,0.,0.866025403784439));
#11313=DIRECTION('',(0.,-1.,0.));
#11314=DIRECTION('',(0.5,0.,0.866025403784439));
#11315=DIRECTION('',(0.,-1.,0.));
#11316=DIRECTION('center_axis',(1.92296268638356E-16,0.,-1.));
#11317=DIRECTION('ref_axis',(1.,0.,1.92296268638356E-16));
#11318=DIRECTION('',(1.,0.,1.92296268638356E-16));
#11319=DIRECTION('',(0.,-1.,0.));
#11320=DIRECTION('',(1.,0.,1.92296268638356E-16));
#11321=DIRECTION('center_axis',(-0.866025403784439,0.,-0.5));
#11322=DIRECTION('ref_axis',(0.5,0.,-0.866025403784439));
#11323=DIRECTION('',(0.5,0.,-0.866025403784439));
#11324=DIRECTION('',(0.,-1.,0.));
#11325=DIRECTION('',(0.5,0.,-0.866025403784438));
#11326=DIRECTION('center_axis',(-0.866025403784439,0.,0.5));
#11327=DIRECTION('ref_axis',(-0.5,0.,-0.866025403784439));
#11328=DIRECTION('',(-0.5,0.,-0.866025403784439));
#11329=DIRECTION('',(0.,-1.,0.));
#11330=DIRECTION('',(-0.5,0.,-0.866025403784439));
#11331=DIRECTION('center_axis',(-1.92296268638356E-16,0.,1.));
#11332=DIRECTION('ref_axis',(-1.,0.,-1.92296268638356E-16));
#11333=DIRECTION('',(-1.,0.,-1.92296268638356E-16));
#11334=DIRECTION('',(0.,-1.,0.));
#11335=DIRECTION('',(-1.,0.,-1.92296268638356E-16));
#11336=DIRECTION('center_axis',(0.866025403784439,0.,0.5));
#11337=DIRECTION('ref_axis',(-0.5,0.,0.866025403784439));
#11338=DIRECTION('',(-0.5,0.,0.866025403784439));
#11339=DIRECTION('',(-0.5,0.,0.866025403784439));
#11340=DIRECTION('center_axis',(0.,-1.,0.));
#11341=DIRECTION('ref_axis',(0.,0.,-1.));
#11342=DIRECTION('center_axis',(0.,1.,0.));
#11343=DIRECTION('ref_axis',(0.,0.,1.));
#11344=DIRECTION('center_axis',(0.,-1.,0.));
#11345=DIRECTION('ref_axis',(1.,0.,0.));
#11346=DIRECTION('center_axis',(0.,-1.,0.));
#11347=DIRECTION('ref_axis',(1.,0.,0.));
#11348=DIRECTION('center_axis',(0.,-1.,0.));
#11349=DIRECTION('ref_axis',(1.,0.,0.));
#11350=DIRECTION('',(0.707106781186547,0.707106781186548,8.65956056235493E-17));
#11351=DIRECTION('center_axis',(0.,-1.,0.));
#11352=DIRECTION('ref_axis',(1.,0.,0.));
#11353=DIRECTION('center_axis',(0.,1.,0.));
#11354=DIRECTION('ref_axis',(1.,0.,0.));
#11355=DIRECTION('',(0.,1.,0.));
#11356=DIRECTION('center_axis',(0.,1.,0.));
#11357=DIRECTION('ref_axis',(1.,0.,0.));
#11358=DIRECTION('center_axis',(0.,-1.,0.));
#11359=DIRECTION('ref_axis',(1.,0.,0.));
#11360=DIRECTION('',(-0.707106781186547,0.707106781186548,-8.65956056235493E-17));
#11361=DIRECTION('center_axis',(0.,-1.,0.));
#11362=DIRECTION('ref_axis',(0.,0.,-1.));
#14387=CARTESIAN_POINT('',(0.,0.,0.));
#14388=CARTESIAN_POINT('Origin',(0.0721687836487032,0.,-0.125));
#14389=CARTESIAN_POINT('',(0.0721687836487032,0.,-0.125));
#14390=CARTESIAN_POINT('',(0.144337567297406,0.,0.));
#14391=CARTESIAN_POINT('',(0.117710979560879,0.,-0.0461186027918559));
#14392=CARTESIAN_POINT('',(0.0721687836487032,-0.25,-0.125));
#14393=CARTESIAN_POINT('',(0.0721687836487032,0.,-0.125));
#14394=CARTESIAN_POINT('',(0.144337567297406,-0.25,0.));
#14395=CARTESIAN_POINT('',(0.144337567297406,-0.25,0.));
#14396=CARTESIAN_POINT('',(0.144337567297406,0.,0.));
#14397=CARTESIAN_POINT('Origin',(-0.0721687836487032,0.,-0.125));
#14398=CARTESIAN_POINT('',(-0.0721687836487032,0.,-0.125));
#14399=CARTESIAN_POINT('',(0.0739156081756484,0.,-0.125));
#14400=CARTESIAN_POINT('',(-0.0721687836487032,-0.25,-0.125));
#14401=CARTESIAN_POINT('',(-0.0721687836487032,0.,-0.125));
#14402=CARTESIAN_POINT('',(0.0721687836487032,-0.25,-0.125));
#14403=CARTESIAN_POINT('Origin',(-0.144337567297406,0.,-4.16333634234434E-17));
#14404=CARTESIAN_POINT('',(-0.144337567297406,0.,-1.76762539787485E-17));
#14405=CARTESIAN_POINT('',(-0.0987953713852306,0.,-0.0788813972081442));
#14406=CARTESIAN_POINT('',(-0.144337567297406,-0.25,-2.77555756156289E-17));
#14407=CARTESIAN_POINT('',(-0.144337567297406,0.,-1.76762539787485E-17));
#14408=CARTESIAN_POINT('',(-0.0721687836487032,-0.25,-0.125));
#14409=CARTESIAN_POINT('Origin',(-0.0721687836487033,0.,0.125));
#14410=CARTESIAN_POINT('',(-0.0721687836487033,0.,0.125));
#14411=CARTESIAN_POINT('',(-0.0627109795608791,0.,0.141381397208144));
#14412=CARTESIAN_POINT('',(-0.0721687836487033,-0.25,0.125));
#14413=CARTESIAN_POINT('',(-0.0721687836487033,0.,0.125));
#14414=CARTESIAN_POINT('',(-0.144337567297406,-0.25,-1.76762539787485E-17));
#14415=CARTESIAN_POINT('Origin',(0.0721687836487032,0.,0.125));
#14416=CARTESIAN_POINT('',(0.0721687836487032,0.,0.125));
#14417=CARTESIAN_POINT('',(0.146084391824352,0.,0.125));
#14418=CARTESIAN_POINT('',(0.0721687836487032,-0.25,0.125));
#14419=CARTESIAN_POINT('',(0.0721687836487032,0.,0.125));
#14420=CARTESIAN_POINT('',(-0.0721687836487033,-0.25,0.125));
#14421=CARTESIAN_POINT('Origin',(0.144337567297406,0.,0.));
#14422=CARTESIAN_POINT('',(0.153795371385231,0.,-0.0163813972081441));
#14423=CARTESIAN_POINT('',(0.0721687836487032,-0.25,0.125));
#14424=CARTESIAN_POINT('Origin',(0.,-0.25,0.));
#14425=CARTESIAN_POINT('Origin',(0.22,0.,0.));
#14426=CARTESIAN_POINT('',(-0.22,-8.67361737988404E-18,-2.69422295812418E-17));
#14427=CARTESIAN_POINT('Origin',(0.,0.,0.));
#14428=CARTESIAN_POINT('Origin',(0.,-0.015,0.));
#14429=CARTESIAN_POINT('',(-0.24505,-0.02505,-3.00099698131059E-17));
#14430=CARTESIAN_POINT('Origin',(0.,-0.02505,0.));
#14431=CARTESIAN_POINT('',(-0.235,-0.015,-2.87791997799628E-17));
#14432=CARTESIAN_POINT('Origin',(0.,-0.3775,0.));
#14433=CARTESIAN_POINT('',(-0.24505,-0.72995,3.00099698131059E-17));
#14434=CARTESIAN_POINT('Origin',(0.,-0.72995,0.));
#14435=CARTESIAN_POINT('',(-0.24505,-0.3775,-3.00099698131059E-17));
#14436=CARTESIAN_POINT('Origin',(0.,-0.7625,0.));
#14437=CARTESIAN_POINT('',(-0.175,-0.8,-2.14313189850787E-17));
#14438=CARTESIAN_POINT('Origin',(0.,-0.8,0.));
#14439=CARTESIAN_POINT('',(-0.2125,-0.7625,-2.60237444818813E-17));
#14440=CARTESIAN_POINT('Origin',(0.,-0.8,0.));
#16163=UNCERTAINTY_MEASURE_WITH_UNIT(LENGTH_MEASURE(0.001),#16282,
'DISTANCE_ACCURACY_VALUE',
'Maximum model space distance between geometric entities at asserted c
onnectivities');
#16212=UNCERTAINTY_MEASURE_WITH_UNIT(LENGTH_MEASURE(0.001),#16282,
'DISTANCE_ACCURACY_VALUE',
'Maximum model space distance between geometric entities at asserted c
onnectivities');
#16232=(
GEOMETRIC_REPRESENTATION_CONTEXT(3)
GLOBAL_UNCERTAINTY_ASSIGNED_CONTEXT((#16163))
GLOBAL_UNIT_ASSIGNED_CONTEXT((#16282,#16284,#16285))
REPRESENTATION_CONTEXT('','3D')
);
#16281=(
GEOMETRIC_REPRESENTATION_CONTEXT(3)
GLOBAL_UNCERTAINTY_ASSIGNED_CONTEXT((#16212))
GLOBAL_UNIT_ASSIGNED_CONTEXT((#16282,#16284,#16285))
REPRESENTATION_CONTEXT('','3D')
);
#16282=(
LENGTH_UNIT()
NAMED_UNIT(*)
SI_UNIT(.CENTI.,.METRE.)
);
#16284=(
NAMED_UNIT(*)
PLANE_ANGLE_UNIT()
SI_UNIT($,.RADIAN.)
);
#16285=(
NAMED_UNIT(*)
SI_UNIT($,.STERADIAN.)
SOLID_ANGLE_UNIT()
);
#16305=SHAPE_DEFINITION_REPRESENTATION(#16392,#16538);
#16392=PRODUCT_DEFINITION_SHAPE('',$,#16607);
#16538=SHAPE_REPRESENTATION('',(#9508),#16232);
#16587=PRODUCT_DEFINITION_CONTEXT('part definition',#16793,'design');
#16607=PRODUCT_DEFINITION('Socket Set Screw - M5x8',
'Socket Set Screw - M5x8',#16675,#16587);
#16675=PRODUCT_DEFINITION_FORMATION('',$,#16814);
#16793=APPLICATION_CONTEXT(
'Core Data for Automotive Mechanical Design Process');
#16794=PRODUCT_CONTEXT('part definition',#16793,'mechanical');
#16814=PRODUCT('Socket Set Screw - M5x8','Socket Set Screw - M5x8',
'Socket Set Screw - M5x8',(#16794));
#16933=COLOUR_RGB('Black',0.12,0.14,0.17);
#16934=FILL_AREA_STYLE_COLOUR('',#16933);
#16935=FILL_AREA_STYLE('',(#16934));
#16936=SURFACE_STYLE_FILL_AREA(#16935);
#16937=SURFACE_SIDE_STYLE('',(#16936));
#16938=SURFACE_STYLE_USAGE(.BOTH.,#16937);
#16939=PRESENTATION_STYLE_ASSIGNMENT((#16938));
ENDSEC;
END-ISO-10303-21;
